ISO-10303-21;
HEADER;
/* Generated by software containing ST-Developer
 * from STEP Tools, Inc. (www.steptools.com) 
 */

FILE_DESCRIPTION(
/* description */ ('Belt tensioner idler arm'),
/* implementation_level */ '2;1');

FILE_NAME(
/* name */ 'Cap Screw - M5x20.step',
/* time_stamp */ '2026-10-28T03:22:15-07:00',
/* author */ (''),
/* organization */ (''),
/* preprocessor_version */ 'ST-DEVELOPER v20.2',
/* originating_system */ 'Autodesk Translation Framework v15.17.0.0',
/* authorisation */ '');

FILE_SCHEMA (('AUTOMOTIVE_DESIGN { 1 0 10303 214 3 1 1 }'));
ENDSEC;

DATA;
#10=MECHANICAL_DESIGN_GEOMETRIC_PRESENTATION_REPRESENTATION('',(#456),#12779);
#285=ORIENTED_CLOSED_SHELL('',*,#6191,.F.);
#289=BREP_WITH_VOIDS('Body1',#6190,(#285));
#294=CONICAL_SURFACE('',#6743,0.4,0.785398163397448);
#295=CONICAL_SURFACE('',#6747,0.41,0.785398163397448);
#296=CONICAL_SURFACE('',#6751,0.26,0.463647609000806);
#297=CONICAL_SURFACE('',#6755,0.225,0.785398163397448);
#388=SHAPE_REPRESENTATION_RELATIONSHIP('SRR','None',#12934,#422);
#422=ADVANCED_BREP_SHAPE_REPRESENTATION('',(#289),#12751);
#456=STYLED_ITEM('',(#13191),#289);
#558=FACE_BOUND('',#1314,.T.);
#710=PLANE('',#6741);
#711=PLANE('',#6749);
#712=PLANE('',#6757);
#713=PLANE('',#6758);
#714=PLANE('',#6759);
#715=PLANE('',#6760);
#716=PLANE('',#6761);
#717=PLANE('',#6762);
#718=PLANE('',#6763);
#719=PLANE('',#6764);
#720=PLANE('',#6765);
#911=FACE_OUTER_BOUND('',#1309,.T.);
#912=FACE_OUTER_BOUND('',#1310,.T.);
#913=FACE_OUTER_BOUND('',#1311,.T.);
#914=FACE_OUTER_BOUND('',#1312,.T.);
#915=FACE_OUTER_BOUND('',#1313,.T.);
#916=FACE_OUTER_BOUND('',#1315,.T.);
#917=FACE_OUTER_BOUND('',#1316,.T.);
#918=FACE_OUTER_BOUND('',#1317,.T.);
#919=FACE_OUTER_BOUND('',#1318,.T.);
#920=FACE_OUTER_BOUND('',#1319,.T.);
#921=FACE_OUTER_BOUND('',#1320,.T.);
#922=FACE_OUTER_BOUND('',#1321,.T.);
#923=FACE_OUTER_BOUND('',#1322,.T.);
#924=FACE_OUTER_BOUND('',#1323,.T.);
#925=FACE_OUTER_BOUND('',#1324,.T.);
#926=FACE_OUTER_BOUND('',#1325,.T.);
#927=FACE_OUTER_BOUND('',#1326,.T.);
#1309=EDGE_LOOP('',(#4376));
#1310=EDGE_LOOP('',(#4377,#4378,#4379,#4380));
#1311=EDGE_LOOP('',(#4381,#4382,#4383,#4384));
#1312=EDGE_LOOP('',(#4385,#4386,#4387,#4388));
#1313=EDGE_LOOP('',(#4389));
#1314=EDGE_LOOP('',(#4390));
#1315=EDGE_LOOP('',(#4391,#4392,#4393,#4394));
#1316=EDGE_LOOP('',(#4395,#4396,#4397,#4398));
#1317=EDGE_LOOP('',(#4399,#4400,#4401,#4402));
#1318=EDGE_LOOP('',(#4403));
#1319=EDGE_LOOP('',(#4404,#4405,#4406,#4407));
#1320=EDGE_LOOP('',(#4408,#4409,#4410,#4411));
#1321=EDGE_LOOP('',(#4412,#4413,#4414,#4415));
#1322=EDGE_LOOP('',(#4416,#4417,#4418,#4419));
#1323=EDGE_LOOP('',(#4420,#4421,#4422,#4423));
#1324=EDGE_LOOP('',(#4424,#4425,#4426,#4427));
#1325=EDGE_LOOP('',(#4428,#4429,#4430,#4431,#4432,#4433));
#1326=EDGE_LOOP('',(#4434,#4435,#4436,#4437,#4438,#4439));
#1786=LINE('',#10477,#2135);
#1787=LINE('',#10481,#2136);
#1788=LINE('',#10485,#2137);
#1789=LINE('',#10492,#2138);
#1790=LINE('',#10496,#2139);
#1791=LINE('',#10500,#2140);
#1792=LINE('',#10505,#2141);
#1793=LINE('',#10507,#2142);
#1794=LINE('',#10509,#2143);
#1795=LINE('',#10510,#2144);
#1796=LINE('',#10513,#2145);
#1797=LINE('',#10515,#2146);
#1798=LINE('',#10516,#2147);
#1799=LINE('',#10519,#2148);
#1800=LINE('',#10521,#2149);
#1801=LINE('',#10522,#2150);
#1802=LINE('',#10525,#2151);
#1803=LINE('',#10527,#2152);
#1804=LINE('',#10528,#2153);
#1805=LINE('',#10531,#2154);
#1806=LINE('',#10533,#2155);
#1807=LINE('',#10534,#2156);
#1808=LINE('',#10536,#2157);
#1809=LINE('',#10537,#2158);
#2135=VECTOR('',#7798,0.4);
#2136=VECTOR('',#7803,0.425);
#2137=VECTOR('',#7808,0.41);
#2138=VECTOR('',#7817,0.26);
#2139=VECTOR('',#7822,0.25);
#2140=VECTOR('',#7827,0.225);
#2141=VECTOR('',#7832,1.);
#2142=VECTOR('',#7833,1.);
#2143=VECTOR('',#7834,1.);
#2144=VECTOR('',#7835,1.);
#2145=VECTOR('',#7838,1.);
#2146=VECTOR('',#7839,1.);
#2147=VECTOR('',#7840,1.);
#2148=VECTOR('',#7843,1.);
#2149=VECTOR('',#7844,1.);
#2150=VECTOR('',#7845,1.);
#2151=VECTOR('',#7848,1.);
#2152=VECTOR('',#7849,1.);
#2153=VECTOR('',#7850,1.);
#2154=VECTOR('',#7853,1.);
#2155=VECTOR('',#7854,1.);
#2156=VECTOR('',#7855,1.);
#2157=VECTOR('',#7858,1.);
#2158=VECTOR('',#7859,1.);
#2458=CIRCLE('',#6742,0.375);
#2459=CIRCLE('',#6744,0.425);
#2460=CIRCLE('',#6746,0.425);
#2461=CIRCLE('',#6748,0.395);
#2462=CIRCLE('',#6750,0.27);
#2463=CIRCLE('',#6752,0.24505);
#2464=CIRCLE('',#6754,0.24505);
#2465=CIRCLE('',#6756,0.2);
#2863=VERTEX_POINT('',#10472);
#2864=VERTEX_POINT('',#10475);
#2865=VERTEX_POINT('',#10479);
#2866=VERTEX_POINT('',#10483);
#2867=VERTEX_POINT('',#10487);
#2868=VERTEX_POINT('',#10490);
#2869=VERTEX_POINT('',#10494);
#2870=VERTEX_POINT('',#10498);
#2871=VERTEX_POINT('',#10503);
#2872=VERTEX_POINT('',#10504);
#2873=VERTEX_POINT('',#10506);
#2874=VERTEX_POINT('',#10508);
#2875=VERTEX_POINT('',#10512);
#2876=VERTEX_POINT('',#10514);
#2877=VERTEX_POINT('',#10518);
#2878=VERTEX_POINT('',#10520);
#2879=VERTEX_POINT('',#10524);
#2880=VERTEX_POINT('',#10526);
#2881=VERTEX_POINT('',#10530);
#2882=VERTEX_POINT('',#10532);
#3443=EDGE_CURVE('',#2863,#2863,#2458,.T.);
#3444=EDGE_CURVE('',#2864,#2864,#2459,.T.);
#3445=EDGE_CURVE('',#2864,#2863,#1786,.T.);
#3446=EDGE_CURVE('',#2865,#2865,#2460,.T.);
#3447=EDGE_CURVE('',#2865,#2864,#1787,.T.);
#3448=EDGE_CURVE('',#2866,#2866,#2461,.T.);
#3449=EDGE_CURVE('',#2866,#2865,#1788,.T.);
#3450=EDGE_CURVE('',#2867,#2867,#2462,.T.);
#3451=EDGE_CURVE('',#2868,#2868,#2463,.F.);
#3452=EDGE_CURVE('',#2868,#2867,#1789,.T.);
#3453=EDGE_CURVE('',#2869,#2869,#2464,.F.);
#3454=EDGE_CURVE('',#2869,#2868,#1790,.T.);
#3455=EDGE_CURVE('',#2870,#2870,#2465,.T.);
#3456=EDGE_CURVE('',#2870,#2869,#1791,.T.);
#3457=EDGE_CURVE('',#2871,#2872,#1792,.T.);
#3458=EDGE_CURVE('',#2872,#2873,#1793,.T.);
#3459=EDGE_CURVE('',#2873,#2874,#1794,.T.);
#3460=EDGE_CURVE('',#2871,#2874,#1795,.T.);
#3461=EDGE_CURVE('',#2872,#2875,#1796,.T.);
#3462=EDGE_CURVE('',#2875,#2876,#1797,.T.);
#3463=EDGE_CURVE('',#2876,#2873,#1798,.T.);
#3464=EDGE_CURVE('',#2875,#2877,#1799,.T.);
#3465=EDGE_CURVE('',#2877,#2878,#1800,.T.);
#3466=EDGE_CURVE('',#2878,#2876,#1801,.T.);
#3467=EDGE_CURVE('',#2877,#2879,#1802,.T.);
#3468=EDGE_CURVE('',#2879,#2880,#1803,.T.);
#3469=EDGE_CURVE('',#2880,#2878,#1804,.T.);
#3470=EDGE_CURVE('',#2879,#2881,#1805,.T.);
#3471=EDGE_CURVE('',#2881,#2882,#1806,.T.);
#3472=EDGE_CURVE('',#2882,#2880,#1807,.T.);
#3473=EDGE_CURVE('',#2881,#2871,#1808,.T.);
#3474=EDGE_CURVE('',#2874,#2882,#1809,.T.);
#4376=ORIENTED_EDGE('',*,*,#3443,.F.);
#4377=ORIENTED_EDGE('',*,*,#3444,.F.);
#4378=ORIENTED_EDGE('',*,*,#3445,.T.);
#4379=ORIENTED_EDGE('',*,*,#3443,.T.);
#4380=ORIENTED_EDGE('',*,*,#3445,.F.);
#4381=ORIENTED_EDGE('',*,*,#3446,.F.);
#4382=ORIENTED_EDGE('',*,*,#3447,.T.);
#4383=ORIENTED_EDGE('',*,*,#3444,.T.);
#4384=ORIENTED_EDGE('',*,*,#3447,.F.);
#4385=ORIENTED_EDGE('',*,*,#3448,.F.);
#4386=ORIENTED_EDGE('',*,*,#3449,.T.);
#4387=ORIENTED_EDGE('',*,*,#3446,.T.);
#4388=ORIENTED_EDGE('',*,*,#3449,.F.);
#4389=ORIENTED_EDGE('',*,*,#3448,.T.);
#4390=ORIENTED_EDGE('',*,*,#3450,.F.);
#4391=ORIENTED_EDGE('',*,*,#3451,.F.);
#4392=ORIENTED_EDGE('',*,*,#3452,.T.);
#4393=ORIENTED_EDGE('',*,*,#3450,.T.);
#4394=ORIENTED_EDGE('',*,*,#3452,.F.);
#4395=ORIENTED_EDGE('',*,*,#3453,.F.);
#4396=ORIENTED_EDGE('',*,*,#3454,.T.);
#4397=ORIENTED_EDGE('',*,*,#3451,.T.);
#4398=ORIENTED_EDGE('',*,*,#3454,.F.);
#4399=ORIENTED_EDGE('',*,*,#3455,.F.);
#4400=ORIENTED_EDGE('',*,*,#3456,.T.);
#4401=ORIENTED_EDGE('',*,*,#3453,.T.);
#4402=ORIENTED_EDGE('',*,*,#3456,.F.);
#4403=ORIENTED_EDGE('',*,*,#3455,.T.);
#4404=ORIENTED_EDGE('',*,*,#3457,.T.);
#4405=ORIENTED_EDGE('',*,*,#3458,.T.);
#4406=ORIENTED_EDGE('',*,*,#3459,.T.);
#4407=ORIENTED_EDGE('',*,*,#3460,.F.);
#4408=ORIENTED_EDGE('',*,*,#3461,.T.);
#4409=ORIENTED_EDGE('',*,*,#3462,.T.);
#4410=ORIENTED_EDGE('',*,*,#3463,.T.);
#4411=ORIENTED_EDGE('',*,*,#3458,.F.);
#4412=ORIENTED_EDGE('',*,*,#3464,.T.);
#4413=ORIENTED_EDGE('',*,*,#3465,.T.);
#4414=ORIENTED_EDGE('',*,*,#3466,.T.);
#4415=ORIENTED_EDGE('',*,*,#3462,.F.);
#4416=ORIENTED_EDGE('',*,*,#3467,.T.);
#4417=ORIENTED_EDGE('',*,*,#3468,.T.);
#4418=ORIENTED_EDGE('',*,*,#3469,.T.);
#4419=ORIENTED_EDGE('',*,*,#3465,.F.);
#4420=ORIENTED_EDGE('',*,*,#3470,.T.);
#4421=ORIENTED_EDGE('',*,*,#3471,.T.);
#4422=ORIENTED_EDGE('',*,*,#3472,.T.);
#4423=ORIENTED_EDGE('',*,*,#3468,.F.);
#4424=ORIENTED_EDGE('',*,*,#3473,.T.);
#4425=ORIENTED_EDGE('',*,*,#3460,.T.);
#4426=ORIENTED_EDGE('',*,*,#3474,.T.);
#4427=ORIENTED_EDGE('',*,*,#3471,.F.);
#4428=ORIENTED_EDGE('',*,*,#3473,.F.);
#4429=ORIENTED_EDGE('',*,*,#3470,.F.);
#4430=ORIENTED_EDGE('',*,*,#3467,.F.);
#4431=ORIENTED_EDGE('',*,*,#3464,.F.);
#4432=ORIENTED_EDGE('',*,*,#3461,.F.);
#4433=ORIENTED_EDGE('',*,*,#3457,.F.);
#4434=ORIENTED_EDGE('',*,*,#3474,.F.);
#4435=ORIENTED_EDGE('',*,*,#3459,.F.);
#4436=ORIENTED_EDGE('',*,*,#3463,.F.);
#4437=ORIENTED_EDGE('',*,*,#3466,.F.);
#4438=ORIENTED_EDGE('',*,*,#3469,.F.);
#4439=ORIENTED_EDGE('',*,*,#3472,.F.);
#5687=CYLINDRICAL_SURFACE('',#6745,0.425);
#5688=CYLINDRICAL_SURFACE('',#6753,0.24505);
#5888=ADVANCED_FACE('',(#911),#710,.T.);
#5889=ADVANCED_FACE('',(#912),#294,.T.);
#5890=ADVANCED_FACE('',(#913),#5687,.T.);
#5891=ADVANCED_FACE('',(#914),#295,.T.);
#5892=ADVANCED_FACE('',(#915,#558),#711,.T.);
#5893=ADVANCED_FACE('',(#916),#296,.T.);
#5894=ADVANCED_FACE('',(#917),#5688,.T.);
#5895=ADVANCED_FACE('',(#918),#297,.T.);
#5896=ADVANCED_FACE('',(#919),#712,.T.);
#5897=ADVANCED_FACE('',(#920),#713,.F.);
#5898=ADVANCED_FACE('',(#921),#714,.F.);
#5899=ADVANCED_FACE('',(#922),#715,.F.);
#5900=ADVANCED_FACE('',(#923),#716,.F.);
#5901=ADVANCED_FACE('',(#924),#717,.F.);
#5902=ADVANCED_FACE('',(#925),#718,.F.);
#5903=ADVANCED_FACE('',(#926),#719,.F.);
#5904=ADVANCED_FACE('',(#927),#720,.F.);
#6190=CLOSED_SHELL('',(#5888,#5889,#5890,#5891,#5892,#5893,#5894,#5895,
#5896));
#6191=CLOSED_SHELL('',(#5897,#5898,#5899,#5900,#5901,#5902,#5903,#5904));
#6740=AXIS2_PLACEMENT_3D('',#10470,#7788,#7789);
#6741=AXIS2_PLACEMENT_3D('',#10471,#7790,#7791);
#6742=AXIS2_PLACEMENT_3D('',#10473,#7792,#7793);
#6743=AXIS2_PLACEMENT_3D('',#10474,#7794,#7795);
#6744=AXIS2_PLACEMENT_3D('',#10476,#7796,#7797);
#6745=AXIS2_PLACEMENT_3D('',#10478,#7799,#7800);
#6746=AXIS2_PLACEMENT_3D('',#10480,#7801,#7802);
#6747=AXIS2_PLACEMENT_3D('',#10482,#7804,#7805);
#6748=AXIS2_PLACEMENT_3D('',#10484,#7806,#7807);
#6749=AXIS2_PLACEMENT_3D('',#10486,#7809,#7810);
#6750=AXIS2_PLACEMENT_3D('',#10488,#7811,#7812);
#6751=AXIS2_PLACEMENT_3D('',#10489,#7813,#7814);
#6752=AXIS2_PLACEMENT_3D('',#10491,#7815,#7816);
#6753=AXIS2_PLACEMENT_3D('',#10493,#7818,#7819);
#6754=AXIS2_PLACEMENT_3D('',#10495,#7820,#7821);
#6755=AXIS2_PLACEMENT_3D('',#10497,#7823,#7824);
#6756=AXIS2_PLACEMENT_3D('',#10499,#7825,#7826);
#6757=AXIS2_PLACEMENT_3D('',#10501,#7828,#7829);
#6758=AXIS2_PLACEMENT_3D('',#10502,#7830,#7831);
#6759=AXIS2_PLACEMENT_3D('',#10511,#7836,#7837);
#6760=AXIS2_PLACEMENT_3D('',#10517,#7841,#7842);
#6761=AXIS2_PLACEMENT_3D('',#10523,#7846,#7847);
#6762=AXIS2_PLACEMENT_3D('',#10529,#7851,#7852);
#6763=AXIS2_PLACEMENT_3D('',#10535,#7856,#7857);
#6764=AXIS2_PLACEMENT_3D('',#10538,#7860,#7861);
#6765=AXIS2_PLACEMENT_3D('',#10539,#7862,#7863);
#7788=DIRECTION('axis',(0.,0.,1.));
#7789=DIRECTION('refdir',(1.,0.,0.));
#7790=DIRECTION('center_axis',(0.,1.,0.));
#7791=DIRECTION('ref_axis',(0.,0.,1.));
#7792=DIRECTION('center_axis',(0.,-1.,0.));
#7793=DIRECTION('ref_axis',(1.,0.,0.));
#7794=DIRECTION('center_axis',(0.,-1.,0.));
#7795=DIRECTION('ref_axis',(1.,0.,0.));
#7796=DIRECTION('center_axis',(0.,-1.,0.));
#7797=DIRECTION('ref_axis',(1.,0.,0.));
#7798=DIRECTION('',(0.707106781186548,0.707106781186547,8.65956056235493E-17));
#7799=DIRECTION('center_axis',(0.,-1.,0.));
#7800=DIRECTION('ref_axis',(1.,0.,0.));
#7801=DIRECTION('center_axis',(0.,-1.,0.));
#7802=DIRECTION('ref_axis',(1.,0.,0.));
#7803=DIRECTION('',(0.,1.,0.));
#7804=DIRECTION('center_axis',(0.,1.,0.));
#7805=DIRECTION('ref_axis',(1.,0.,0.));
#7806=DIRECTION('center_axis',(0.,-1.,0.));
#7807=DIRECTION('ref_axis',(1.,0.,0.));
#7808=DIRECTION('',(-0.707106781186547,0.707106781186548,-8.65956056235493E-17));
#7809=DIRECTION('center_axis',(0.,-1.,0.));
#7810=DIRECTION('ref_axis',(0.,0.,-1.));
#7811=DIRECTION('center_axis',(0.,-1.,0.));
#7812=DIRECTION('ref_axis',(1.,0.,0.));
#7813=DIRECTION('center_axis',(0.,1.,0.));
#7814=DIRECTION('ref_axis',(1.,0.,0.));
#7815=DIRECTION('center_axis',(0.,1.,0.));
#7816=DIRECTION('ref_axis',(1.,0.,0.));
#7817=DIRECTION('',(-0.447213595499958,0.894427190999916,-5.47678698264203E-17));
#7818=DIRECTION('center_axis',(0.,-1.,0.));
#7819=DIRECTION('ref_axis',(1.,0.,0.));
#7820=DIRECTION('center_axis',(0.,1.,0.));
#7821=DIRECTION('ref_axis',(1.,0.,0.));
#7822=DIRECTION('',(0.,1.,0.));
#7823=DIRECTION('center_axis',(0.,1.,0.));
#7824=DIRECTION('ref_axis',(1.,0.,0.));
#7825=DIRECTION('center_axis',(0.,-1.,0.));
#7826=DIRECTION('ref_axis',(1.,0.,0.));
#7827=DIRECTION('',(-0.707106781186547,0.707106781186548,-8.65956056235493E-17));
#7828=DIRECTION('center_axis',(0.,-1.,0.));
#7829=DIRECTION('ref_axis',(0.,0.,-1.));
#7830=DIRECTION('center_axis',(0.866025403784439,0.,-0.5));
#7831=DIRECTION('ref_axis',(0.5,0.,0.866025403784439));
#7832=DIRECTION('',(-0.5,0.,-0.866025403784439));
#7833=DIRECTION('',(0.,-1.,0.));
#7834=DIRECTION('',(0.5,0.,0.866025403784439));
#7835=DIRECTION('',(0.,-1.,0.));
#7836=DIRECTION('center_axis',(1.20185167898973E-16,0.,-1.));
#7837=DIRECTION('ref_axis',(1.,0.,1.20185167898973E-16));
#7838=DIRECTION('',(-1.,0.,-1.20185167898973E-16));
#7839=DIRECTION('',(0.,-1.,0.));
#7840=DIRECTION('',(1.,0.,1.20185167898973E-16));
#7841=DIRECTION('center_axis',(-0.866025403784439,0.,-0.5));
#7842=DIRECTION('ref_axis',(0.5,0.,-0.866025403784439));
#7843=DIRECTION('',(-0.5,0.,0.866025403784439));
#7844=DIRECTION('',(0.,-1.,0.));
#7845=DIRECTION('',(0.5,0.,-0.866025403784439));
#7846=DIRECTION('center_axis',(-0.866025403784439,0.,0.5));
#7847=DIRECTION('ref_axis',(-0.5,0.,-0.866025403784439));
#7848=DIRECTION('',(0.5,0.,0.866025403784439));
#7849=DIRECTION('',(0.,-1.,0.));
#7850=DIRECTION('',(-0.5,0.,-0.866025403784439));
#7851=DIRECTION('center_axis',(-2.40370335797945E-16,0.,1.));
#7852=DIRECTION('ref_axis',(-1.,0.,-2.40370335797945E-16));
#7853=DIRECTION('',(1.,0.,2.40370335797945E-16));
#7854=DIRECTION('',(0.,-1.,0.));
#7855=DIRECTION('',(-1.,0.,-2.40370335797945E-16));
#7856=DIRECTION('center_axis',(0.866025403784439,0.,0.5));
#7857=DIRECTION('ref_axis',(-0.5,0.,0.866025403784439));
#7858=DIRECTION('',(0.5,0.,-0.866025403784439));
#7859=DIRECTION('',(-0.5,0.,0.866025403784439));
#7860=DIRECTION('center_axis',(0.,1.,0.));
#7861=DIRECTION('ref_axis',(1.,0.,0.));
#7862=DIRECTION('center_axis',(0.,-1.,0.));
#7863=DIRECTION('ref_axis',(0.,0.,-1.));
#10470=CARTESIAN_POINT('',(0.,0.,0.));
#10471=CARTESIAN_POINT('Origin',(0.375,0.5,0.));
#10472=CARTESIAN_POINT('',(-0.375,0.5,-4.59242549680257E-17));
#10473=CARTESIAN_POINT('Origin',(0.,0.5,0.));
#10474=CARTESIAN_POINT('Origin',(0.,0.475,0.));
#10475=CARTESIAN_POINT('',(-0.425,0.45,-5.20474889637625E-17));
#10476=CARTESIAN_POINT('Origin',(0.,0.45,0.));
#10477=CARTESIAN_POINT('',(-0.4,0.475,-4.89858719658941E-17));
#10478=CARTESIAN_POINT('Origin',(0.,0.24,0.));
#10479=CARTESIAN_POINT('',(-0.425,0.0299999999999998,-5.20474889637625E-17));
#10480=CARTESIAN_POINT('Origin',(0.,0.0299999999999998,0.));
#10481=CARTESIAN_POINT('',(-0.425,0.24,-5.20474889637625E-17));
#10482=CARTESIAN_POINT('Origin',(0.,0.0150000000000001,0.));
#10483=CARTESIAN_POINT('',(-0.395,4.85722573273506E-17,-4.83735485663204E-17));
#10484=CARTESIAN_POINT('Origin',(0.,0.,0.));
#10485=CARTESIAN_POINT('',(-0.41,0.0150000000000001,-5.02105187650415E-17));
#10486=CARTESIAN_POINT('Origin',(0.27,0.,0.));
#10487=CARTESIAN_POINT('',(-0.27,0.,-3.30654635769785E-17));
#10488=CARTESIAN_POINT('Origin',(0.,0.,0.));
#10489=CARTESIAN_POINT('Origin',(0.,-0.02,0.));
#10490=CARTESIAN_POINT('',(-0.24505,-0.0498999999999999,3.00099698131059E-17));
#10491=CARTESIAN_POINT('Origin',(0.,-0.0498999999999999,0.));
#10492=CARTESIAN_POINT('',(-0.26,-0.02,-3.18408167778312E-17));
#10493=CARTESIAN_POINT('Origin',(0.,-0.995,0.));
#10494=CARTESIAN_POINT('',(-0.24505,-1.95495,3.00099698131059E-17));
#10495=CARTESIAN_POINT('Origin',(0.,-1.95495,0.));
#10496=CARTESIAN_POINT('',(-0.24505,-0.995,-3.00099698131059E-17));
#10497=CARTESIAN_POINT('Origin',(0.,-1.975,0.));
#10498=CARTESIAN_POINT('',(-0.2,-2.,-2.44929359829471E-17));
#10499=CARTESIAN_POINT('Origin',(0.,-2.,0.));
#10500=CARTESIAN_POINT('',(-0.225,-1.975,-2.75545529808154E-17));
#10501=CARTESIAN_POINT('Origin',(0.,-2.,0.));
#10502=CARTESIAN_POINT('Origin',(0.115470053837925,-0.5,-0.2));
#10503=CARTESIAN_POINT('',(0.23094010767585,-0.5,0.));
#10504=CARTESIAN_POINT('',(0.115470053837925,-0.5,-0.2));
#10505=CARTESIAN_POINT('',(0.23094010767585,-0.5,0.));
#10506=CARTESIAN_POINT('',(0.115470053837925,-0.8,-0.2));
#10507=CARTESIAN_POINT('',(0.115470053837925,-0.5,-0.2));
#10508=CARTESIAN_POINT('',(0.23094010767585,-0.8,0.));
#10509=CARTESIAN_POINT('',(0.23094010767585,-0.8,0.));
#10510=CARTESIAN_POINT('',(0.23094010767585,-0.5,0.));
#10511=CARTESIAN_POINT('Origin',(-0.115470053837925,-0.5,-0.2));
#10512=CARTESIAN_POINT('',(-0.115470053837925,-0.5,-0.2));
#10513=CARTESIAN_POINT('',(0.115470053837925,-0.5,-0.2));
#10514=CARTESIAN_POINT('',(-0.115470053837925,-0.8,-0.2));
#10515=CARTESIAN_POINT('',(-0.115470053837925,-0.5,-0.2));
#10516=CARTESIAN_POINT('',(0.115470053837925,-0.8,-0.2));
#10517=CARTESIAN_POINT('Origin',(-0.23094010767585,-0.5,-2.77555756156289E-17));
#10518=CARTESIAN_POINT('',(-0.23094010767585,-0.5,-2.82820063659975E-17));
#10519=CARTESIAN_POINT('',(-0.115470053837925,-0.5,-0.2));
#10520=CARTESIAN_POINT('',(-0.23094010767585,-0.8,-2.77555756156289E-17));
#10521=CARTESIAN_POINT('',(-0.23094010767585,-0.5,-2.82820063659975E-17));
#10522=CARTESIAN_POINT('',(-0.115470053837925,-0.8,-0.2));
#10523=CARTESIAN_POINT('Origin',(-0.115470053837925,-0.5,0.2));
#10524=CARTESIAN_POINT('',(-0.115470053837925,-0.5,0.2));
#10525=CARTESIAN_POINT('',(-0.23094010767585,-0.5,-2.82820063659975E-17));
#10526=CARTESIAN_POINT('',(-0.115470053837925,-0.8,0.2));
#10527=CARTESIAN_POINT('',(-0.115470053837925,-0.5,0.2));
#10528=CARTESIAN_POINT('',(-0.23094010767585,-0.8,-2.82820063659975E-17));
#10529=CARTESIAN_POINT('Origin',(0.115470053837925,-0.5,0.2));
#10530=CARTESIAN_POINT('',(0.115470053837925,-0.5,0.2));
#10531=CARTESIAN_POINT('',(-0.115470053837925,-0.5,0.2));
#10532=CARTESIAN_POINT('',(0.115470053837925,-0.8,0.2));
#10533=CARTESIAN_POINT('',(0.115470053837925,-0.5,0.2));
#10534=CARTESIAN_POINT('',(-0.115470053837925,-0.8,0.2));
#10535=CARTESIAN_POINT('Origin',(0.23094010767585,-0.5,0.));
#10536=CARTESIAN_POINT('',(0.115470053837925,-0.5,0.2));
#10537=CARTESIAN_POINT('',(0.115470053837925,-0.8,0.2));
#10538=CARTESIAN_POINT('Origin',(0.,-0.5,0.));
#10539=CARTESIAN_POINT('Origin',(0.,-0.8,0.));
#12711=UNCERTAINTY_MEASURE_WITH_UNIT(LENGTH_MEASURE(0.001),#12780,
'DISTANCE_ACCURACY_VALUE',
'Maximum model space distance between geometric entities at asserted c
onnectivities');
#12739=UNCERTAINTY_MEASURE_WITH_UNIT(LENGTH_MEASURE(0.001),#12780,
'DISTANCE_ACCURACY_VALUE',
'Maximum model space distance between geometric entities at asserted c
onnectivities');
#12751=(
GEOMETRIC_REPRESENTATION_CONTEXT(3)
GLOBAL_UNCERTAINTY_ASSIGNED_CONTEXT((#12711))
GLOBAL_UNIT_ASSIGNED_CONTEXT((#12780,#12782,#12783))
REPRESENTATION_CONTEXT('','3D')
);
#12779=(
GEOMETRIC_REPRESENTATION_CONTEXT(3)
GLOBAL_UNCERTAINTY_ASSIGNED_CONTEXT((#12739))
GLOBAL_UNIT_ASSIGNED_CONTEXT((#12780,#12782,#12783))
REPRESENTATION_CONTEXT('','3D')
);
#12780=(
LENGTH_UNIT()
NAMED_UNIT(*)
SI_UNIT(.CENTI.,.METRE.)
);
#12782=(
NAMED_UNIT(*)
PLANE_ANGLE_UNIT()
SI_UNIT($,.RADIAN.)
);
#12783=(
NAMED_UNIT(*)
SI_UNIT($,.STERADIAN.)
SOLID_ANGLE_UNIT()
);
#12795=SHAPE_DEFINITION_REPRESENTATION(#12834,#12934);
#12834=PRODUCT_DEFINITION_SHAPE('',$,#12974);
#12934=SHAPE_REPRESENTATION('',(#6740),#12751);
#12962=PRODUCT_DEFINITION_CONTEXT('part definition',#13081,'design');
#12974=PRODUCT_DEFINITION('Cap Screw - M5x20','Cap Screw - M5x20',#13013,
#12962);
#13013=PRODUCT_DEFINITION_FORMATION('',$,#13094);
#13081=APPLICATION_CONTEXT(
'Core Data for Automotive Mechanical Design Process');
#13082=PRODUCT_CONTEXT('part definition',#13081,'mechanical');
#13094=PRODUCT('Cap Screw - M5x20','Cap Screw - M5x20',
'Cap Screw - M5x20',(#13082));
#13185=COLOUR_RGB('Black',0.12,0.14,0.17);
#13186=FILL_AREA_STYLE_COLOUR('',#13185);
#13187=FILL_AREA_STYLE('',(#13186));
#13188=SURFACE_STYLE_FILL_AREA(#13187);
#13189=SURFACE_SIDE_STYLE('',(#13188));
#13190=SURFACE_STYLE_USAGE(.BOTH.,#13189);
#13191=PRESENTATION_STYLE_ASSIGNMENT((#13190));
ENDSEC;
END-ISO-10303-21;
